ISO-10303-21;
HEADER;
/* Generated by software containing ST-Developer
 * from STEP Tools, Inc. (www.steptools.com) 
 */

FILE_DESCRIPTION(
/* description */ ('Grid plate located blocks and clamp'),
/* implementation_level */ '2;1');

FILE_NAME(
/* name */ 'Replaceable contact pad.step',
/* time_stamp */ '2026-10-29T15:43:47-07:00',
/* author */ (''),
/* organization */ (''),
/* preprocessor_version */ 'ST-DEVELOPER v20.2',
/* originating_system */ 'Autodesk Translation Framework v15.17.0.0',
/* authorisation */ '');

FILE_SCHEMA (('AUTOMOTIVE_DESIGN { 1 0 10303 214 3 1 1 }'));
ENDSEC;

DATA;
#10=MECHANICAL_DESIGN_GEOMETRIC_PRESENTATION_REPRESENTATION('',(#173),#5702);
#147=SHAPE_REPRESENTATION_RELATIONSHIP('SRR','None',#5765,#159);
#159=ADVANCED_BREP_SHAPE_REPRESENTATION('',(#186),#5695);
#173=STYLED_ITEM('',(#5890),#186);
#186=MANIFOLD_SOLID_BREP('Body1',#3269);
#258=FACE_BOUND('',#830,.T.);
#259=FACE_BOUND('',#831,.T.);
#346=CIRCLE('',#3612,0.164999999999999);
#347=CIRCLE('',#3613,0.164999999999999);
#348=CIRCLE('',#3616,0.164999999999999);
#349=CIRCLE('',#3617,0.164999999999999);
#350=CIRCLE('',#3620,1.5);
#351=CIRCLE('',#3621,1.5);
#434=CYLINDRICAL_SURFACE('',#3611,0.164999999999999);
#435=CYLINDRICAL_SURFACE('',#3615,0.164999999999999);
#436=CYLINDRICAL_SURFACE('',#3619,1.5);
#571=FACE_OUTER_BOUND('',#820,.T.);
#572=FACE_OUTER_BOUND('',#821,.T.);
#573=FACE_OUTER_BOUND('',#822,.T.);
#574=FACE_OUTER_BOUND('',#823,.T.);
#575=FACE_OUTER_BOUND('',#824,.T.);
#576=FACE_OUTER_BOUND('',#825,.T.);
#577=FACE_OUTER_BOUND('',#826,.T.);
#578=FACE_OUTER_BOUND('',#827,.T.);
#579=FACE_OUTER_BOUND('',#828,.T.);
#580=FACE_OUTER_BOUND('',#829,.T.);
#820=EDGE_LOOP('',(#2680,#2681,#2682,#2683));
#821=EDGE_LOOP('',(#2684));
#822=EDGE_LOOP('',(#2685,#2686,#2687,#2688));
#823=EDGE_LOOP('',(#2689));
#824=EDGE_LOOP('',(#2690,#2691,#2692,#2693));
#825=EDGE_LOOP('',(#2694,#2695,#2696,#2697));
#826=EDGE_LOOP('',(#2698,#2699,#2700,#2701));
#827=EDGE_LOOP('',(#2702,#2703,#2704,#2705));
#828=EDGE_LOOP('',(#2706,#2707,#2708,#2709));
#829=EDGE_LOOP('',(#2710,#2711,#2712,#2713));
#830=EDGE_LOOP('',(#2714));
#831=EDGE_LOOP('',(#2715));
#1093=LINE('',#5319,#1366);
#1094=LINE('',#5326,#1367);
#1095=LINE('',#5332,#1368);
#1096=LINE('',#5336,#1369);
#1097=LINE('',#5340,#1370);
#1098=LINE('',#5342,#1371);
#1099=LINE('',#5343,#1372);
#1100=LINE('',#5346,#1373);
#1101=LINE('',#5347,#1374);
#1102=LINE('',#5350,#1375);
#1103=LINE('',#5351,#1376);
#1104=LINE('',#5353,#1377);
#1366=VECTOR('',#4363,0.164999999999999);
#1367=VECTOR('',#4372,0.164999999999999);
#1368=VECTOR('',#4379,1.);
#1369=VECTOR('',#4382,1.);
#1370=VECTOR('',#4387,1.);
#1371=VECTOR('',#4388,1.);
#1372=VECTOR('',#4389,1.);
#1373=VECTOR('',#4392,1.);
#1374=VECTOR('',#4393,1.);
#1375=VECTOR('',#4396,1.);
#1376=VECTOR('',#4397,1.);
#1377=VECTOR('',#4400,1.);
#1623=VERTEX_POINT('',#5316);
#1624=VERTEX_POINT('',#5318);
#1625=VERTEX_POINT('',#5323);
#1626=VERTEX_POINT('',#5325);
#1627=VERTEX_POINT('',#5330);
#1628=VERTEX_POINT('',#5331);
#1629=VERTEX_POINT('',#5333);
#1630=VERTEX_POINT('',#5335);
#1631=VERTEX_POINT('',#5339);
#1632=VERTEX_POINT('',#5341);
#1633=VERTEX_POINT('',#5345);
#1634=VERTEX_POINT('',#5349);
#1990=EDGE_CURVE('',#1623,#1623,#346,.T.);
#1991=EDGE_CURVE('',#1623,#1624,#1093,.T.);
#1992=EDGE_CURVE('',#1624,#1624,#347,.T.);
#1993=EDGE_CURVE('',#1625,#1625,#348,.T.);
#1994=EDGE_CURVE('',#1625,#1626,#1094,.T.);
#1995=EDGE_CURVE('',#1626,#1626,#349,.T.);
#1996=EDGE_CURVE('',#1627,#1628,#1095,.T.);
#1997=EDGE_CURVE('',#1629,#1627,#350,.T.);
#1998=EDGE_CURVE('',#1630,#1629,#1096,.T.);
#1999=EDGE_CURVE('',#1628,#1630,#351,.T.);
#2000=EDGE_CURVE('',#1627,#1631,#1097,.T.);
#2001=EDGE_CURVE('',#1632,#1631,#1098,.T.);
#2002=EDGE_CURVE('',#1629,#1632,#1099,.T.);
#2003=EDGE_CURVE('',#1628,#1633,#1100,.T.);
#2004=EDGE_CURVE('',#1631,#1633,#1101,.T.);
#2005=EDGE_CURVE('',#1634,#1632,#1102,.T.);
#2006=EDGE_CURVE('',#1630,#1634,#1103,.T.);
#2007=EDGE_CURVE('',#1633,#1634,#1104,.T.);
#2680=ORIENTED_EDGE('',*,*,#1990,.F.);
#2681=ORIENTED_EDGE('',*,*,#1991,.T.);
#2682=ORIENTED_EDGE('',*,*,#1992,.F.);
#2683=ORIENTED_EDGE('',*,*,#1991,.F.);
#2684=ORIENTED_EDGE('',*,*,#1990,.T.);
#2685=ORIENTED_EDGE('',*,*,#1993,.F.);
#2686=ORIENTED_EDGE('',*,*,#1994,.T.);
#2687=ORIENTED_EDGE('',*,*,#1995,.F.);
#2688=ORIENTED_EDGE('',*,*,#1994,.F.);
#2689=ORIENTED_EDGE('',*,*,#1993,.T.);
#2690=ORIENTED_EDGE('',*,*,#1996,.F.);
#2691=ORIENTED_EDGE('',*,*,#1997,.F.);
#2692=ORIENTED_EDGE('',*,*,#1998,.F.);
#2693=ORIENTED_EDGE('',*,*,#1999,.F.);
#2694=ORIENTED_EDGE('',*,*,#1997,.T.);
#2695=ORIENTED_EDGE('',*,*,#2000,.T.);
#2696=ORIENTED_EDGE('',*,*,#2001,.F.);
#2697=ORIENTED_EDGE('',*,*,#2002,.F.);
#2698=ORIENTED_EDGE('',*,*,#1996,.T.);
#2699=ORIENTED_EDGE('',*,*,#2003,.T.);
#2700=ORIENTED_EDGE('',*,*,#2004,.F.);
#2701=ORIENTED_EDGE('',*,*,#2000,.F.);
#2702=ORIENTED_EDGE('',*,*,#1998,.T.);
#2703=ORIENTED_EDGE('',*,*,#2002,.T.);
#2704=ORIENTED_EDGE('',*,*,#2005,.F.);
#2705=ORIENTED_EDGE('',*,*,#2006,.F.);
#2706=ORIENTED_EDGE('',*,*,#1999,.T.);
#2707=ORIENTED_EDGE('',*,*,#2006,.T.);
#2708=ORIENTED_EDGE('',*,*,#2007,.F.);
#2709=ORIENTED_EDGE('',*,*,#2003,.F.);
#2710=ORIENTED_EDGE('',*,*,#2007,.T.);
#2711=ORIENTED_EDGE('',*,*,#2005,.T.);
#2712=ORIENTED_EDGE('',*,*,#2001,.T.);
#2713=ORIENTED_EDGE('',*,*,#2004,.T.);
#2714=ORIENTED_EDGE('',*,*,#1992,.T.);
#2715=ORIENTED_EDGE('',*,*,#1995,.T.);
#3037=PLANE('',#3614);
#3038=PLANE('',#3618);
#3039=PLANE('',#3622);
#3040=PLANE('',#3623);
#3041=PLANE('',#3624);
#3042=PLANE('',#3625);
#3043=PLANE('',#3626);
#3192=ADVANCED_FACE('',(#571),#434,.F.);
#3193=ADVANCED_FACE('',(#572),#3037,.T.);
#3194=ADVANCED_FACE('',(#573),#435,.F.);
#3195=ADVANCED_FACE('',(#574),#3038,.T.);
#3196=ADVANCED_FACE('',(#575),#436,.F.);
#3197=ADVANCED_FACE('',(#576),#3039,.T.);
#3198=ADVANCED_FACE('',(#577),#3040,.T.);
#3199=ADVANCED_FACE('',(#578),#3041,.T.);
#3200=ADVANCED_FACE('',(#579),#3042,.T.);
#3201=ADVANCED_FACE('',(#580,#258,#259),#3043,.T.);
#3269=CLOSED_SHELL('',(#3192,#3193,#3194,#3195,#3196,#3197,#3198,#3199,
#3200,#3201));
#3610=AXIS2_PLACEMENT_3D('',#5314,#4357,#4358);
#3611=AXIS2_PLACEMENT_3D('',#5315,#4359,#4360);
#3612=AXIS2_PLACEMENT_3D('',#5317,#4361,#4362);
#3613=AXIS2_PLACEMENT_3D('',#5320,#4364,#4365);
#3614=AXIS2_PLACEMENT_3D('',#5321,#4366,#4367);
#3615=AXIS2_PLACEMENT_3D('',#5322,#4368,#4369);
#3616=AXIS2_PLACEMENT_3D('',#5324,#4370,#4371);
#3617=AXIS2_PLACEMENT_3D('',#5327,#4373,#4374);
#3618=AXIS2_PLACEMENT_3D('',#5328,#4375,#4376);
#3619=AXIS2_PLACEMENT_3D('',#5329,#4377,#4378);
#3620=AXIS2_PLACEMENT_3D('',#5334,#4380,#4381);
#3621=AXIS2_PLACEMENT_3D('',#5337,#4383,#4384);
#3622=AXIS2_PLACEMENT_3D('',#5338,#4385,#4386);
#3623=AXIS2_PLACEMENT_3D('',#5344,#4390,#4391);
#3624=AXIS2_PLACEMENT_3D('',#5348,#4394,#4395);
#3625=AXIS2_PLACEMENT_3D('',#5352,#4398,#4399);
#3626=AXIS2_PLACEMENT_3D('',#5354,#4401,#4402);
#4357=DIRECTION('axis',(0.,0.,1.));
#4358=DIRECTION('refdir',(1.,0.,0.));
#4359=DIRECTION('center_axis',(0.,0.,1.));
#4360=DIRECTION('ref_axis',(1.,0.,0.));
#4361=DIRECTION('center_axis',(0.,0.,1.));
#4362=DIRECTION('ref_axis',(1.,0.,0.));
#4363=DIRECTION('',(0.,0.,1.));
#4364=DIRECTION('center_axis',(0.,0.,-1.));
#4365=DIRECTION('ref_axis',(1.,0.,0.));
#4366=DIRECTION('center_axis',(0.,0.,1.));
#4367=DIRECTION('ref_axis',(1.,0.,0.));
#4368=DIRECTION('center_axis',(0.,0.,1.));
#4369=DIRECTION('ref_axis',(1.,0.,0.));
#4370=DIRECTION('center_axis',(0.,0.,1.));
#4371=DIRECTION('ref_axis',(1.,0.,0.));
#4372=DIRECTION('',(0.,0.,1.));
#4373=DIRECTION('center_axis',(0.,0.,-1.));
#4374=DIRECTION('ref_axis',(1.,0.,0.));
#4375=DIRECTION('center_axis',(0.,0.,1.));
#4376=DIRECTION('ref_axis',(1.,0.,0.));
#4377=DIRECTION('center_axis',(1.,0.,0.));
#4378=DIRECTION('ref_axis',(0.,1.22464679914735E-16,1.));
#4379=DIRECTION('',(-1.,0.,0.));
#4380=DIRECTION('center_axis',(-1.,0.,0.));
#4381=DIRECTION('ref_axis',(0.,0.,-1.));
#4382=DIRECTION('',(1.,0.,0.));
#4383=DIRECTION('center_axis',(1.,0.,0.));
#4384=DIRECTION('ref_axis',(0.,0.,-1.));
#4385=DIRECTION('center_axis',(1.,0.,0.));
#4386=DIRECTION('ref_axis',(0.,1.,0.));
#4387=DIRECTION('',(0.,0.,1.));
#4388=DIRECTION('',(0.,1.,0.));
#4389=DIRECTION('',(0.,0.,1.));
#4390=DIRECTION('center_axis',(0.,1.,0.));
#4391=DIRECTION('ref_axis',(-1.,0.,0.));
#4392=DIRECTION('',(0.,0.,1.));
#4393=DIRECTION('',(-1.,0.,0.));
#4394=DIRECTION('center_axis',(0.,-1.,0.));
#4395=DIRECTION('ref_axis',(1.,0.,0.));
#4396=DIRECTION('',(1.,0.,0.));
#4397=DIRECTION('',(0.,0.,1.));
#4398=DIRECTION('center_axis',(-1.,0.,0.));
#4399=DIRECTION('ref_axis',(0.,-1.,0.));
#4400=DIRECTION('',(0.,-1.,0.));
#4401=DIRECTION('center_axis',(0.,0.,1.));
#4402=DIRECTION('ref_axis',(1.,0.,0.));
#5314=CARTESIAN_POINT('',(0.,0.,0.));
#5315=CARTESIAN_POINT('Origin',(10.,-0.8,6.02132034));
#5316=CARTESIAN_POINT('',(9.835,-0.8,6.02132034));
#5317=CARTESIAN_POINT('Origin',(10.,-0.8,6.02132034));
#5318=CARTESIAN_POINT('',(9.835,-0.8,6.52132034));
#5319=CARTESIAN_POINT('',(9.835,-0.8,6.02132034));
#5320=CARTESIAN_POINT('Origin',(10.,-0.8,6.52132034));
#5321=CARTESIAN_POINT('Origin',(10.,-0.8,6.02132034));
#5322=CARTESIAN_POINT('Origin',(10.,0.8,6.02132034));
#5323=CARTESIAN_POINT('',(9.835,0.8,6.02132034));
#5324=CARTESIAN_POINT('Origin',(10.,0.8,6.02132034));
#5325=CARTESIAN_POINT('',(9.835,0.8,6.52132034));
#5326=CARTESIAN_POINT('',(9.835,0.8,6.02132034));
#5327=CARTESIAN_POINT('Origin',(10.,0.8,6.52132034));
#5328=CARTESIAN_POINT('Origin',(10.,0.8,6.02132034));
#5329=CARTESIAN_POINT('Origin',(8.9,0.,4.62132034355964));
#5330=CARTESIAN_POINT('',(11.,1.2,5.52132034));
#5331=CARTESIAN_POINT('',(9.,1.2,5.52132034));
#5332=CARTESIAN_POINT('',(11.,1.2,5.52132034));
#5333=CARTESIAN_POINT('',(11.,-1.2,5.52132034));
#5334=CARTESIAN_POINT('Origin',(11.,0.,4.62132034355964));
#5335=CARTESIAN_POINT('',(9.,-1.2,5.52132034));
#5336=CARTESIAN_POINT('',(9.,-1.2,5.52132034));
#5337=CARTESIAN_POINT('Origin',(9.,0.,4.62132034355964));
#5338=CARTESIAN_POINT('Origin',(11.,-1.2,5.52132034));
#5339=CARTESIAN_POINT('',(11.,1.2,6.52132034));
#5340=CARTESIAN_POINT('',(11.,1.2,5.52132034));
#5341=CARTESIAN_POINT('',(11.,-1.2,6.52132034));
#5342=CARTESIAN_POINT('',(11.,-1.2,6.52132034));
#5343=CARTESIAN_POINT('',(11.,-1.2,5.52132034));
#5344=CARTESIAN_POINT('Origin',(11.,1.2,5.52132034));
#5345=CARTESIAN_POINT('',(9.,1.2,6.52132034));
#5346=CARTESIAN_POINT('',(9.,1.2,5.52132034));
#5347=CARTESIAN_POINT('',(11.,1.2,6.52132034));
#5348=CARTESIAN_POINT('Origin',(9.,-1.2,5.52132034));
#5349=CARTESIAN_POINT('',(9.,-1.2,6.52132034));
#5350=CARTESIAN_POINT('',(9.,-1.2,6.52132034));
#5351=CARTESIAN_POINT('',(9.,-1.2,5.52132034));
#5352=CARTESIAN_POINT('Origin',(9.,1.2,5.52132034));
#5353=CARTESIAN_POINT('',(9.,1.2,6.52132034));
#5354=CARTESIAN_POINT('Origin',(10.,0.,6.52132034));
#5681=UNCERTAINTY_MEASURE_WITH_UNIT(LENGTH_MEASURE(0.001),#5703,
'DISTANCE_ACCURACY_VALUE',
'Maximum model space distance between geometric entities at asserted c
onnectivities');
#5688=UNCERTAINTY_MEASURE_WITH_UNIT(LENGTH_MEASURE(0.001),#5703,
'DISTANCE_ACCURACY_VALUE',
'Maximum model space distance between geometric entities at asserted c
onnectivities');
#5695=(
GEOMETRIC_REPRESENTATION_CONTEXT(3)
GLOBAL_UNCERTAINTY_ASSIGNED_CONTEXT((#5681))
GLOBAL_UNIT_ASSIGNED_CONTEXT((#5703,#5705,#5706))
REPRESENTATION_CONTEXT('','3D')
);
#5702=(
GEOMETRIC_REPRESENTATION_CONTEXT(3)
GLOBAL_UNCERTAINTY_ASSIGNED_CONTEXT((#5688))
GLOBAL_UNIT_ASSIGNED_CONTEXT((#5703,#5705,#5706))
REPRESENTATION_CONTEXT('','3D')
);
#5703=(
LENGTH_UNIT()
NAMED_UNIT(*)
SI_UNIT(.CENTI.,.METRE.)
);
#5705=(
NAMED_UNIT(*)
PLANE_ANGLE_UNIT()
SI_UNIT($,.RADIAN.)
);
#5706=(
NAMED_UNIT(*)
SI_UNIT($,.STERADIAN.)
SOLID_ANGLE_UNIT()
);
#5713=SHAPE_DEFINITION_REPRESENTATION(#5726,#5765);
#5726=PRODUCT_DEFINITION_SHAPE('',$,#5779);
#5765=SHAPE_REPRESENTATION('',(#3610),#5695);
#5772=PRODUCT_DEFINITION_CONTEXT('part definition',#5813,'design');
#5779=PRODUCT_DEFINITION('Replaceable contact pad',
'Replaceable contact pad',#5792,#5772);
#5792=PRODUCT_DEFINITION_FORMATION('',$,#5821);
#5813=APPLICATION_CONTEXT(
'Core Data for Automotive Mechanical Design Process');
#5814=PRODUCT_CONTEXT('part definition',#5813,'mechanical');
#5821=PRODUCT('Replaceable contact pad','Replaceable contact pad',
'Replaceable contact pad',(#5814));
#5884=COLOUR_RGB('Sky Blue',0.24,0.69,0.87);
#5885=FILL_AREA_STYLE_COLOUR('',#5884);
#5886=FILL_AREA_STYLE('',(#5885));
#5887=SURFACE_STYLE_FILL_AREA(#5886);
#5888=SURFACE_SIDE_STYLE('',(#5887));
#5889=SURFACE_STYLE_USAGE(.BOTH.,#5888);
#5890=PRESENTATION_STYLE_ASSIGNMENT((#5889));
ENDSEC;
END-ISO-10303-21;
